ISO-10303-21;
HEADER;
/* Generated by software containing ST-Developer
 * from STEP Tools, Inc. (www.steptools.com) 
 */

FILE_DESCRIPTION(
/* description */ ('Located fixture plate with toggle clamp'),
/* implementation_level */ '2;1');

FILE_NAME(
/* name */ 'Bolted edge stop.step',
/* time_stamp */ '2026-10-27T21:36:12-07:00',
/* author */ (''),
/* organization */ (''),
/* preprocessor_version */ 'ST-DEVELOPER v20.2',
/* originating_system */ 'Autodesk Translation Framework v15.17.0.0',
/* authorisation */ '');

FILE_SCHEMA (('AUTOMOTIVE_DESIGN { 1 0 10303 214 3 1 1 }'));
ENDSEC;

DATA;
#10=MECHANICAL_DESIGN_GEOMETRIC_PRESENTATION_REPRESENTATION('',(#326),#9285);
#278=SHAPE_REPRESENTATION_RELATIONSHIP('SRR','None',#9401,#302);
#302=ADVANCED_BREP_SHAPE_REPRESENTATION('',(#349),#9263);
#326=STYLED_ITEM('',(#9619),#349);
#349=MANIFOLD_SOLID_BREP('Body1',#5175);
#444=FACE_BOUND('',#1162,.T.);
#445=FACE_BOUND('',#1163,.T.);
#446=FACE_BOUND('',#1166,.T.);
#447=FACE_BOUND('',#1167,.T.);
#551=PLANE('',#5679);
#552=PLANE('',#5680);
#553=PLANE('',#5681);
#554=PLANE('',#5682);
#555=PLANE('',#5683);
#556=PLANE('',#5684);
#785=FACE_OUTER_BOUND('',#1158,.T.);
#786=FACE_OUTER_BOUND('',#1159,.T.);
#787=FACE_OUTER_BOUND('',#1160,.T.);
#788=FACE_OUTER_BOUND('',#1161,.T.);
#789=FACE_OUTER_BOUND('',#1164,.T.);
#790=FACE_OUTER_BOUND('',#1165,.T.);
#791=FACE_OUTER_BOUND('',#1168,.T.);
#792=FACE_OUTER_BOUND('',#1169,.T.);
#1158=EDGE_LOOP('',(#4040,#4041,#4042,#4043));
#1159=EDGE_LOOP('',(#4044,#4045,#4046,#4047));
#1160=EDGE_LOOP('',(#4048,#4049,#4050,#4051));
#1161=EDGE_LOOP('',(#4052,#4053,#4054,#4055));
#1162=EDGE_LOOP('',(#4056));
#1163=EDGE_LOOP('',(#4057));
#1164=EDGE_LOOP('',(#4058,#4059,#4060,#4061));
#1165=EDGE_LOOP('',(#4062,#4063,#4064,#4065));
#1166=EDGE_LOOP('',(#4066));
#1167=EDGE_LOOP('',(#4067));
#1168=EDGE_LOOP('',(#4068,#4069,#4070,#4071));
#1169=EDGE_LOOP('',(#4072,#4073,#4074,#4075));
#1475=CIRCLE('',#5674,0.425);
#1476=CIRCLE('',#5675,0.425);
#1477=CIRCLE('',#5677,0.425);
#1478=CIRCLE('',#5678,0.425);
#1767=LINE('',#8161,#2177);
#1768=LINE('',#8167,#2178);
#1769=LINE('',#8172,#2179);
#1770=LINE('',#8174,#2180);
#1771=LINE('',#8176,#2181);
#1772=LINE('',#8177,#2182);
#1773=LINE('',#8180,#2183);
#1774=LINE('',#8182,#2184);
#1775=LINE('',#8183,#2185);
#1776=LINE('',#8186,#2186);
#1777=LINE('',#8188,#2187);
#1778=LINE('',#8189,#2188);
#1779=LINE('',#8191,#2189);
#1780=LINE('',#8192,#2190);
#2177=VECTOR('',#6643,0.425);
#2178=VECTOR('',#6650,0.425);
#2179=VECTOR('',#6655,1.);
#2180=VECTOR('',#6656,1.);
#2181=VECTOR('',#6657,1.);
#2182=VECTOR('',#6658,1.);
#2183=VECTOR('',#6661,1.);
#2184=VECTOR('',#6662,1.);
#2185=VECTOR('',#6663,1.);
#2186=VECTOR('',#6666,1.);
#2187=VECTOR('',#6667,1.);
#2188=VECTOR('',#6668,1.);
#2189=VECTOR('',#6671,1.);
#2190=VECTOR('',#6672,1.);
#2585=VERTEX_POINT('',#8158);
#2586=VERTEX_POINT('',#8160);
#2587=VERTEX_POINT('',#8164);
#2588=VERTEX_POINT('',#8166);
#2589=VERTEX_POINT('',#8170);
#2590=VERTEX_POINT('',#8171);
#2591=VERTEX_POINT('',#8173);
#2592=VERTEX_POINT('',#8175);
#2593=VERTEX_POINT('',#8179);
#2594=VERTEX_POINT('',#8181);
#2595=VERTEX_POINT('',#8185);
#2596=VERTEX_POINT('',#8187);
#3108=EDGE_CURVE('',#2585,#2585,#1475,.T.);
#3109=EDGE_CURVE('',#2585,#2586,#1767,.T.);
#3110=EDGE_CURVE('',#2586,#2586,#1476,.T.);
#3111=EDGE_CURVE('',#2587,#2587,#1477,.T.);
#3112=EDGE_CURVE('',#2587,#2588,#1768,.T.);
#3113=EDGE_CURVE('',#2588,#2588,#1478,.T.);
#3114=EDGE_CURVE('',#2589,#2590,#1769,.T.);
#3115=EDGE_CURVE('',#2590,#2591,#1770,.T.);
#3116=EDGE_CURVE('',#2592,#2591,#1771,.T.);
#3117=EDGE_CURVE('',#2589,#2592,#1772,.T.);
#3118=EDGE_CURVE('',#2593,#2589,#1773,.T.);
#3119=EDGE_CURVE('',#2594,#2592,#1774,.T.);
#3120=EDGE_CURVE('',#2593,#2594,#1775,.T.);
#3121=EDGE_CURVE('',#2595,#2593,#1776,.T.);
#3122=EDGE_CURVE('',#2596,#2594,#1777,.T.);
#3123=EDGE_CURVE('',#2595,#2596,#1778,.T.);
#3124=EDGE_CURVE('',#2590,#2595,#1779,.T.);
#3125=EDGE_CURVE('',#2591,#2596,#1780,.T.);
#4040=ORIENTED_EDGE('',*,*,#3108,.F.);
#4041=ORIENTED_EDGE('',*,*,#3109,.T.);
#4042=ORIENTED_EDGE('',*,*,#3110,.F.);
#4043=ORIENTED_EDGE('',*,*,#3109,.F.);
#4044=ORIENTED_EDGE('',*,*,#3111,.F.);
#4045=ORIENTED_EDGE('',*,*,#3112,.T.);
#4046=ORIENTED_EDGE('',*,*,#3113,.F.);
#4047=ORIENTED_EDGE('',*,*,#3112,.F.);
#4048=ORIENTED_EDGE('',*,*,#3114,.T.);
#4049=ORIENTED_EDGE('',*,*,#3115,.T.);
#4050=ORIENTED_EDGE('',*,*,#3116,.F.);
#4051=ORIENTED_EDGE('',*,*,#3117,.F.);
#4052=ORIENTED_EDGE('',*,*,#3118,.T.);
#4053=ORIENTED_EDGE('',*,*,#3117,.T.);
#4054=ORIENTED_EDGE('',*,*,#3119,.F.);
#4055=ORIENTED_EDGE('',*,*,#3120,.F.);
#4056=ORIENTED_EDGE('',*,*,#3110,.T.);
#4057=ORIENTED_EDGE('',*,*,#3113,.T.);
#4058=ORIENTED_EDGE('',*,*,#3121,.T.);
#4059=ORIENTED_EDGE('',*,*,#3120,.T.);
#4060=ORIENTED_EDGE('',*,*,#3122,.F.);
#4061=ORIENTED_EDGE('',*,*,#3123,.F.);
#4062=ORIENTED_EDGE('',*,*,#3124,.T.);
#4063=ORIENTED_EDGE('',*,*,#3123,.T.);
#4064=ORIENTED_EDGE('',*,*,#3125,.F.);
#4065=ORIENTED_EDGE('',*,*,#3115,.F.);
#4066=ORIENTED_EDGE('',*,*,#3108,.T.);
#4067=ORIENTED_EDGE('',*,*,#3111,.T.);
#4068=ORIENTED_EDGE('',*,*,#3125,.T.);
#4069=ORIENTED_EDGE('',*,*,#3122,.T.);
#4070=ORIENTED_EDGE('',*,*,#3119,.T.);
#4071=ORIENTED_EDGE('',*,*,#3116,.T.);
#4072=ORIENTED_EDGE('',*,*,#3124,.F.);
#4073=ORIENTED_EDGE('',*,*,#3114,.F.);
#4074=ORIENTED_EDGE('',*,*,#3118,.F.);
#4075=ORIENTED_EDGE('',*,*,#3121,.F.);
#4835=CYLINDRICAL_SURFACE('',#5673,0.425);
#4836=CYLINDRICAL_SURFACE('',#5676,0.425);
#4986=ADVANCED_FACE('',(#785),#4835,.F.);
#4987=ADVANCED_FACE('',(#786),#4836,.F.);
#4988=ADVANCED_FACE('',(#787),#551,.T.);
#4989=ADVANCED_FACE('',(#788,#444,#445),#552,.T.);
#4990=ADVANCED_FACE('',(#789),#553,.T.);
#4991=ADVANCED_FACE('',(#790,#446,#447),#554,.T.);
#4992=ADVANCED_FACE('',(#791),#555,.T.);
#4993=ADVANCED_FACE('',(#792),#556,.F.);
#5175=CLOSED_SHELL('',(#4986,#4987,#4988,#4989,#4990,#4991,#4992,#4993));
#5672=AXIS2_PLACEMENT_3D('',#8156,#6637,#6638);
#5673=AXIS2_PLACEMENT_3D('',#8157,#6639,#6640);
#5674=AXIS2_PLACEMENT_3D('',#8159,#6641,#6642);
#5675=AXIS2_PLACEMENT_3D('',#8162,#6644,#6645);
#5676=AXIS2_PLACEMENT_3D('',#8163,#6646,#6647);
#5677=AXIS2_PLACEMENT_3D('',#8165,#6648,#6649);
#5678=AXIS2_PLACEMENT_3D('',#8168,#6651,#6652);
#5679=AXIS2_PLACEMENT_3D('',#8169,#6653,#6654);
#5680=AXIS2_PLACEMENT_3D('',#8178,#6659,#6660);
#5681=AXIS2_PLACEMENT_3D('',#8184,#6664,#6665);
#5682=AXIS2_PLACEMENT_3D('',#8190,#6669,#6670);
#5683=AXIS2_PLACEMENT_3D('',#8193,#6673,#6674);
#5684=AXIS2_PLACEMENT_3D('',#8194,#6675,#6676);
#6637=DIRECTION('axis',(0.,0.,1.));
#6638=DIRECTION('refdir',(1.,0.,0.));
#6639=DIRECTION('center_axis',(1.,0.,0.));
#6640=DIRECTION('ref_axis',(0.,0.,-1.));
#6641=DIRECTION('center_axis',(1.,0.,0.));
#6642=DIRECTION('ref_axis',(0.,0.,-1.));
#6643=DIRECTION('',(1.,0.,0.));
#6644=DIRECTION('center_axis',(-1.,0.,0.));
#6645=DIRECTION('ref_axis',(0.,0.,-1.));
#6646=DIRECTION('center_axis',(1.,0.,0.));
#6647=DIRECTION('ref_axis',(0.,0.,-1.));
#6648=DIRECTION('center_axis',(1.,0.,0.));
#6649=DIRECTION('ref_axis',(0.,0.,-1.));
#6650=DIRECTION('',(1.,0.,0.));
#6651=DIRECTION('center_axis',(-1.,0.,0.));
#6652=DIRECTION('ref_axis',(0.,0.,-1.));
#6653=DIRECTION('center_axis',(0.,1.,0.));
#6654=DIRECTION('ref_axis',(-1.,0.,0.));
#6655=DIRECTION('',(-1.,0.,0.));
#6656=DIRECTION('',(0.,0.,1.));
#6657=DIRECTION('',(-1.,0.,0.));
#6658=DIRECTION('',(0.,0.,1.));
#6659=DIRECTION('center_axis',(1.,0.,0.));
#6660=DIRECTION('ref_axis',(0.,1.,0.));
#6661=DIRECTION('',(0.,1.,0.));
#6662=DIRECTION('',(0.,1.,0.));
#6663=DIRECTION('',(0.,0.,1.));
#6664=DIRECTION('center_axis',(0.,-1.,0.));
#6665=DIRECTION('ref_axis',(1.,0.,0.));
#6666=DIRECTION('',(1.,0.,0.));
#6667=DIRECTION('',(1.,0.,0.));
#6668=DIRECTION('',(0.,0.,1.));
#6669=DIRECTION('center_axis',(-1.,0.,0.));
#6670=DIRECTION('ref_axis',(0.,-1.,0.));
#6671=DIRECTION('',(0.,-1.,0.));
#6672=DIRECTION('',(0.,-1.,0.));
#6673=DIRECTION('center_axis',(0.,0.,1.));
#6674=DIRECTION('ref_axis',(1.,0.,0.));
#6675=DIRECTION('center_axis',(0.,0.,1.));
#6676=DIRECTION('ref_axis',(1.,0.,0.));
#8156=CARTESIAN_POINT('',(0.,0.,0.));
#8157=CARTESIAN_POINT('Origin',(17.7,5.,4.5));
#8158=CARTESIAN_POINT('',(17.8,5.,4.925));
#8159=CARTESIAN_POINT('Origin',(17.8,5.,4.5));
#8160=CARTESIAN_POINT('',(18.8,5.,4.925));
#8161=CARTESIAN_POINT('',(17.7,5.,4.925));
#8162=CARTESIAN_POINT('Origin',(18.8,5.,4.5));
#8163=CARTESIAN_POINT('Origin',(17.7,5.,7.));
#8164=CARTESIAN_POINT('',(17.8,5.,7.425));
#8165=CARTESIAN_POINT('Origin',(17.8,5.,7.));
#8166=CARTESIAN_POINT('',(18.8,5.,7.425));
#8167=CARTESIAN_POINT('',(17.7,5.,7.425));
#8168=CARTESIAN_POINT('Origin',(18.8,5.,7.));
#8169=CARTESIAN_POINT('Origin',(18.8,5.5,3.5));
#8170=CARTESIAN_POINT('',(18.8,5.5,3.5));
#8171=CARTESIAN_POINT('',(17.8,5.5,3.5));
#8172=CARTESIAN_POINT('',(18.8,5.5,3.5));
#8173=CARTESIAN_POINT('',(17.8,5.5,8.5));
#8174=CARTESIAN_POINT('',(17.8,5.5,3.5));
#8175=CARTESIAN_POINT('',(18.8,5.5,8.5));
#8176=CARTESIAN_POINT('',(18.8,5.5,8.5));
#8177=CARTESIAN_POINT('',(18.8,5.5,3.5));
#8178=CARTESIAN_POINT('Origin',(18.8,4.5,3.5));
#8179=CARTESIAN_POINT('',(18.8,4.5,3.5));
#8180=CARTESIAN_POINT('',(18.8,4.5,3.5));
#8181=CARTESIAN_POINT('',(18.8,4.5,8.5));
#8182=CARTESIAN_POINT('',(18.8,4.5,8.5));
#8183=CARTESIAN_POINT('',(18.8,4.5,3.5));
#8184=CARTESIAN_POINT('Origin',(17.8,4.5,3.5));
#8185=CARTESIAN_POINT('',(17.8,4.5,3.5));
#8186=CARTESIAN_POINT('',(17.8,4.5,3.5));
#8187=CARTESIAN_POINT('',(17.8,4.5,8.5));
#8188=CARTESIAN_POINT('',(17.8,4.5,8.5));
#8189=CARTESIAN_POINT('',(17.8,4.5,3.5));
#8190=CARTESIAN_POINT('Origin',(17.8,5.5,3.5));
#8191=CARTESIAN_POINT('',(17.8,5.5,3.5));
#8192=CARTESIAN_POINT('',(17.8,5.5,8.5));
#8193=CARTESIAN_POINT('Origin',(18.3,5.,8.5));
#8194=CARTESIAN_POINT('Origin',(18.3,5.,3.5));
#9233=UNCERTAINTY_MEASURE_WITH_UNIT(LENGTH_MEASURE(0.001),#9286,
'DISTANCE_ACCURACY_VALUE',
'Maximum model space distance between geometric entities at asserted c
onnectivities');
#9255=UNCERTAINTY_MEASURE_WITH_UNIT(LENGTH_MEASURE(0.001),#9286,
'DISTANCE_ACCURACY_VALUE',
'Maximum model space distance between geometric entities at asserted c
onnectivities');
#9263=(
GEOMETRIC_REPRESENTATION_CONTEXT(3)
GLOBAL_UNCERTAINTY_ASSIGNED_CONTEXT((#9233))
GLOBAL_UNIT_ASSIGNED_CONTEXT((#9286,#9288,#9289))
REPRESENTATION_CONTEXT('','3D')
);
#9285=(
GEOMETRIC_REPRESENTATION_CONTEXT(3)
GLOBAL_UNCERTAINTY_ASSIGNED_CONTEXT((#9255))
GLOBAL_UNIT_ASSIGNED_CONTEXT((#9286,#9288,#9289))
REPRESENTATION_CONTEXT('','3D')
);
#9286=(
LENGTH_UNIT()
NAMED_UNIT(*)
SI_UNIT(.CENTI.,.METRE.)
);
#9288=(
NAMED_UNIT(*)
PLANE_ANGLE_UNIT()
SI_UNIT($,.RADIAN.)
);
#9289=(
NAMED_UNIT(*)
SI_UNIT($,.STERADIAN.)
SOLID_ANGLE_UNIT()
);
#9297=SHAPE_DEFINITION_REPRESENTATION(#9326,#9401);
#9326=PRODUCT_DEFINITION_SHAPE('',$,#9431);
#9401=SHAPE_REPRESENTATION('',(#5672),#9263);
#9423=PRODUCT_DEFINITION_CONTEXT('part definition',#9512,'design');
#9431=PRODUCT_DEFINITION('Bolted edge stop','Bolted edge stop',#9460,#9423);
#9460=PRODUCT_DEFINITION_FORMATION('',$,#9521);
#9512=APPLICATION_CONTEXT(
'Core Data for Automotive Mechanical Design Process');
#9513=PRODUCT_CONTEXT('part definition',#9512,'mechanical');
#9521=PRODUCT('Bolted edge stop','Bolted edge stop','Bolted edge stop',
(#9513));
#9613=COLOUR_RGB('Black',0.12,0.14,0.17);
#9614=FILL_AREA_STYLE_COLOUR('',#9613);
#9615=FILL_AREA_STYLE('',(#9614));
#9616=SURFACE_STYLE_FILL_AREA(#9615);
#9617=SURFACE_SIDE_STYLE('',(#9616));
#9618=SURFACE_STYLE_USAGE(.BOTH.,#9617);
#9619=PRESENTATION_STYLE_ASSIGNMENT((#9618));
ENDSEC;
END-ISO-10303-21;
